ISO-10303-21;
HEADER;
FILE_DESCRIPTION (('STEP AP214'),
    '1' );
FILE_NAME ('Hinge 2.step',
    '2026-10-26T17:37:43',
    ( '' ),
    ( '' ),
    'SwSTEP 2.0',
    'SolidWorks 2024',
    '' );
FILE_SCHEMA (( 'AUTOMOTIVE_DESIGN' ));
ENDSEC;

DATA;
#25=DIRECTION ( 'NONE',  ( 1.000000000000000000, 0.000000000000000000, 3.996303350731721563E-14 ) ) ;
#114=ORIENTED_EDGE ( 'NONE', *, *, #1797, .F. ) ;
#134=CARTESIAN_POINT ( 'NONE',  ( 15.49601198374999989, -3578.946622428999945, 2257.950097350999840 ) ) ;
#136=CARTESIAN_POINT ( 'NONE',  ( 9.970491213060000746, -3580.312548418000006, 2257.932969814999979 ) ) ;
#324=CARTESIAN_POINT ( 'NONE',  ( 12.70000000000000107, -3570.287499999999909, 2279.817639999999756 ) ) ;
#365=ORIENTED_EDGE ( 'NONE', *, *, #11427, .T. ) ;
#447=ORIENTED_EDGE ( 'NONE', *, *, #18326, .F. ) ;
#484=DIRECTION ( 'NONE',  ( 0.000000000000000000, 1.000000000000000000, 0.000000000000000000 ) ) ;
#528=FACE_OUTER_BOUND ( 'NONE', #10890, .T. ) ;
#532=DIRECTION ( 'NONE',  ( 0.000000000000000000, 0.000000000000000000, -1.000000000000000000 ) ) ;
#583=CARTESIAN_POINT ( 'NONE',  ( 11.61864837389999927, -3576.858790609000152, 2257.644359388999874 ) ) ;
#698=VERTEX_POINT ( 'NONE', #22418 ) ;
#737=DIRECTION ( 'NONE',  ( 0.000000000000000000, -1.000000000000000000, 0.000000000000000000 ) ) ;
#742=EDGE_CURVE ( 'NONE', #4653, #946, #14644, .T. ) ;
#784=EDGE_LOOP ( 'NONE', ( #6046, #14713, #447, #10205, #13619, #10680, #15703, #15282 ) ) ;
#810=CARTESIAN_POINT ( 'NONE',  ( 12.69999999999999929, -3589.528000000000247, 2268.705139999999574 ) ) ;
#860=ORIENTED_EDGE ( 'NONE', *, *, #20397, .T. ) ;
#878=DIRECTION ( 'NONE',  ( 0.000000000000000000, -1.000000000000000000, 0.000000000000000000 ) ) ;
#886=LINE ( 'NONE', #16728, #13299 ) ;
#941=LINE ( 'NONE', #22041, #7424 ) ;
#946=VERTEX_POINT ( 'NONE', #12588 ) ;
#966=CIRCLE ( 'NONE', #14083, 6.349999999999855760 ) ;
#1004=PLANE ( 'NONE',  #9161 ) ;
#1120=DIRECTION ( 'NONE',  ( 0.000000000000000000, 1.000000000000000000, 0.000000000000000000 ) ) ;
#1137=CARTESIAN_POINT ( 'NONE',  ( 14.27720943205999937, -3581.868154638000306, 2257.704281108000032 ) ) ;
#1206=CARTESIAN_POINT ( 'NONE',  ( 10.06338274650999942, -3580.575356121999903, 2257.909778189000008 ) ) ;
#1316=PRODUCT_DEFINITION_SHAPE ( 'NONE', 'NONE',  #20503 ) ;
#1376=CARTESIAN_POINT ( 'NONE',  ( 15.21766708706000060, -3580.829381831999854, 2257.881320499000140 ) ) ;
#1418=CARTESIAN_POINT ( 'NONE',  ( 12.97550722921000066, -3576.659101291999832, 2257.594923726999696 ) ) ;
#1485=( GEOMETRIC_REPRESENTATION_CONTEXT ( 3 ) GLOBAL_UNCERTAINTY_ASSIGNED_CONTEXT ( ( #20035 ) ) GLOBAL_UNIT_ASSIGNED_CONTEXT ( ( #19015, #6484, #13749 ) ) REPRESENTATION_CONTEXT ( 'NONE', 'WORKASPACE' ) );
#1488=ADVANCED_FACE ( 'NONE', ( #13471 ), #6444, .T. ) ;
#1562=AXIS2_PLACEMENT_3D ( 'NONE', #810, #22367, #22246 ) ;
#1569=B_SPLINE_CURVE_WITH_KNOTS ( 'NONE', 3,
 ( #22774, #19748, #7546, #17977 ),
 .UNSPECIFIED., .F., .F.,
 ( 4, 4 ),
 ( 0.000000000000000000, 3.168591426078754222E-06 ),
 .UNSPECIFIED. ) ;
#1636=DIRECTION ( 'NONE',  ( 0.000000000000000000, 1.000000000000000000, 0.000000000000000000 ) ) ;
#1645=CARTESIAN_POINT ( 'NONE',  ( 15.54479972196000048, -3579.494985918000111, 2257.962943248000101 ) ) ;
#1694=VERTEX_POINT ( 'NONE', #19333 ) ;
#1773=CARTESIAN_POINT ( 'NONE',  ( 15.42952381853999988, -3578.677498958000342, 2257.932973515999947 ) ) ;
#1797=EDGE_CURVE ( 'NONE', #13900, #7881, #22878, .T. ) ;
#1881=CARTESIAN_POINT ( 'NONE',  ( 15.54479972196000048, -3579.403078500999982, 2257.962943248000101 ) ) ;
#2092=CIRCLE ( 'NONE', #3956, 7.111999999999785160 ) ;
#2096=EDGE_LOOP ( 'NONE', ( #19011, #14789, #7651, #15840 ) ) ;
#2118=CARTESIAN_POINT ( 'NONE',  ( 9.903987878842999137, -3578.946623412000008, 2257.950097015999745 ) ) ;
#2125=CARTESIAN_POINT ( 'NONE',  ( 10.32639513556999944, -3581.071539618999850, 2257.848705702999723 ) ) ;
#2238=CARTESIAN_POINT ( 'NONE',  ( 10.68478392833999990, -3581.509597157999906, 2257.776259854999807 ) ) ;
#2257=( GEOMETRIC_REPRESENTATION_CONTEXT ( 3 ) GLOBAL_UNCERTAINTY_ASSIGNED_CONTEXT ( ( #16741 ) ) GLOBAL_UNIT_ASSIGNED_CONTEXT ( ( #21126, #3419, #23094 ) ) REPRESENTATION_CONTEXT ( 'NONE', 'WORKASPACE' ) );
#2289=ORIENTED_EDGE ( 'NONE', *, *, #2624, .T. ) ;
#2396=FACE_OUTER_BOUND ( 'NONE', #5982, .T. ) ;
#2565=CARTESIAN_POINT ( 'NONE',  ( 10.32641459757000035, -3577.918429336999907, 2257.848701351999807 ) ) ;
#2606=CARTESIAN_POINT ( 'NONE',  ( 0.000000000000000000, 0.000000000000000000, 0.000000000000000000 ) ) ;
#2615=DIRECTION ( 'NONE',  ( 0.000000000000000000, 0.000000000000000000, -1.000000000000000000 ) ) ;
#2624=EDGE_CURVE ( 'NONE', #14130, #16669, #6475, .T. ) ;
#2677=FACE_OUTER_BOUND ( 'NONE', #6298, .T. ) ;
#2714=CARTESIAN_POINT ( 'NONE',  ( 12.70000000000000107, -3589.528000000000247, 2275.817139999999654 ) ) ;
#2728=PLANE ( 'NONE',  #18624 ) ;
#2792=CARTESIAN_POINT ( 'NONE',  ( 12.69999999999999929, -3590.289999999999964, 2268.705139999999574 ) ) ;
#2880=CIRCLE ( 'NONE', #15982, 7.111999999999785160 ) ;
#2894=CARTESIAN_POINT ( 'NONE',  ( 12.70000000000000107, -3590.289999999999964, 2279.817639999999756 ) ) ;
#2897=DIRECTION ( 'NONE',  ( 0.000000000000000000, 0.000000000000000000, -1.000000000000000000 ) ) ;
#2963=AXIS2_PLACEMENT_3D ( 'NONE', #5360, #3819, #14156 ) ;
#3061=EDGE_CURVE ( 'NONE', #15010, #1694, #17490, .T. ) ;
#3131=ORIENTED_EDGE ( 'NONE', *, *, #20397, .F. ) ;
#3168=CARTESIAN_POINT ( 'NONE',  ( 13.24918551347000140, -3576.699137200999758, 2257.605105471000115 ) ) ;
#3190=CARTESIAN_POINT ( 'NONE',  ( 12.69999999999999929, -3590.289999999999964, 2268.705139999999574 ) ) ;
#3247=ORIENTED_EDGE ( 'NONE', *, *, #11813, .T. ) ;
#3252=CARTESIAN_POINT ( 'NONE',  ( 14.71507054554999883, -3581.509743952999997, 2257.776232814999730 ) ) ;
#3340=DIRECTION ( 'NONE',  ( 0.000000000000000000, 0.000000000000000000, 1.000000000000000000 ) ) ;
#3345=CARTESIAN_POINT ( 'NONE',  ( 12.69999999999999929, -3579.494999999999891, 2272.030000000000200 ) ) ;
#3419=( NAMED_UNIT ( * ) PLANE_ANGLE_UNIT ( ) SI_UNIT ( $, .RADIAN. ) );
#3502=ADVANCED_FACE ( 'NONE', ( #528 ), #10736, .F. ) ;
#3564=AXIS2_PLACEMENT_3D ( 'NONE', #9359, #7826, #22111 ) ;
#3585=AXIS2_PLACEMENT_3D ( 'NONE', #19438, #20849, #13821 ) ;
#3590=DIRECTION ( 'NONE',  ( 0.000000000000000000, 0.000000000000000000, 1.000000000000000000 ) ) ;
#3606=CARTESIAN_POINT ( 'NONE',  ( 12.70000020906999971, -3582.339800010000090, 2257.592639999999847 ) ) ;
#3678=ORIENTED_EDGE ( 'NONE', *, *, #13410, .T. ) ;
#3695=DIRECTION ( 'NONE',  ( 0.000000000000000000, 0.000000000000000000, -1.000000000000000000 ) ) ;
#3730=PRODUCT_DEFINITION_FORMATION_WITH_SPECIFIED_SOURCE ( 'ANY', '', #7149, .NOT_KNOWN. ) ;
#3819=DIRECTION ( 'NONE',  ( 0.000000000000000000, -1.000000000000000000, 0.000000000000000000 ) ) ;
#3956=AXIS2_PLACEMENT_3D ( 'NONE', #8400, #1120, #8279 ) ;
#3994=CARTESIAN_POINT ( 'NONE',  ( 12.60780787143999859, -3582.339800030000333, 2257.592639999999847 ) ) ;
#4192=AXIS2_PLACEMENT_3D ( 'NONE', #10650, #5390, #7516 ) ;
#4274=ORIENTED_EDGE ( 'NONE', *, *, #3061, .F. ) ;
#4327=CARTESIAN_POINT ( 'NONE',  ( 15.54479972194844528, -3579.494995305039538, 2257.962943247996918 ) ) ;
#4380=CARTESIAN_POINT ( 'NONE',  ( 12.69999999999999929, -3579.494999999999891, 2272.030000000000200 ) ) ;
#4505=B_SPLINE_CURVE_WITH_KNOTS ( 'NONE', 3,
 ( #9711, #16625, #16403, #20271, #20048, #583, #7736, #11351, #14654, #20376, #14888, #2565, #5874, #9266, #12889, #2118, #21795, #9603, #22017 ),
 .UNSPECIFIED., .F., .F.,
 ( 4, 1, 1, 1, 1, 1, 1, 1, 1, 1, 1, 1, 1, 1, 1, 1, 4 ),
 ( 0.000000000000000000, 0.06250000000000000000, 0.1250000000000000000, 0.1875000000000000000, 0.2500000000000000000, 0.3125000000000000000, 0.3750000000000000000, 0.4375000000000000000, 0.5000000000000000000, 0.5625000000000000000, 0.6250000000000000000, 0.6875000000000000000, 0.7500000000000000000, 0.8125000000000000000, 0.8750000000000000000, 0.9375000000000000000, 1.000000000000000000 ),
 .UNSPECIFIED. ) ;
#4518=ORIENTED_EDGE ( 'NONE', *, *, #17655, .T. ) ;
#4546=DIRECTION ( 'NONE',  ( 0.000000000000000000, -1.000000000000000000, 0.000000000000000000 ) ) ;
#4563=PRODUCT_DEFINITION_CONTEXT ( 'detailed design', #12493, 'design' ) ;
#4576=EDGE_CURVE ( 'NONE', #14130, #12971, #8887, .T. ) ;
#4594=SHAPE_REPRESENTATION_RELATIONSHIP ( 'NONE' , 'NONE' ,  #13255, #19426 ) ;
#4653=VERTEX_POINT ( 'NONE', #12859 ) ;
#4723=DIRECTION ( 'NONE',  ( 1.000000000000000000, 0.000000000000000000, 3.996303350731721563E-14 ) ) ;
#4771=DIRECTION ( 'NONE',  ( 0.000000000000000000, -1.000000000000000000, 0.000000000000000000 ) ) ;
#4781=CARTESIAN_POINT ( 'NONE',  ( 15.07352087697999998, -3581.071667653000077, 2257.848687205999795 ) ) ;
#4871=DIRECTION ( 'NONE',  ( 0.000000000000000000, 0.000000000000000000, -1.000000000000000000 ) ) ;
#5121=CARTESIAN_POINT ( 'NONE',  ( 9.855200508393231473, -3579.494999998446929, 2257.962940200991852 ) ) ;
#5232=DIRECTION ( 'NONE',  ( 1.000000000000000000, 0.000000000000000000, 3.996303350731721563E-14 ) ) ;
#5239=ADVANCED_FACE ( 'NONE', ( #7899, #8018 ), #2728, .T. ) ;
#5360=CARTESIAN_POINT ( 'NONE',  ( 12.69999999999999929, -3583.940000000000055, 2268.705139999999574 ) ) ;
#5390=DIRECTION ( 'NONE',  ( 0.000000000000000000, -1.000000000000000000, 0.000000000000000000 ) ) ;
#5459=AXIS2_PLACEMENT_3D ( 'NONE', #2714, #8004, #9642 ) ;
#5488=B_SPLINE_CURVE_WITH_KNOTS ( 'NONE', 3,
 ( #15330, #19194, #11805, #6549, #11927, #8646, #6898, #1137, #13809, #3252, #10281, #4781, #1376, #11680, #22459, #13688, #6432, #13569, #20710 ),
 .UNSPECIFIED., .F., .F.,
 ( 4, 1, 1, 1, 1, 1, 1, 1, 1, 1, 1, 1, 1, 1, 1, 1, 4 ),
 ( 0.000000000000000000, 0.06250000000000000000, 0.1250000000000000000, 0.1875000000000000000, 0.2500000000000000000, 0.3125000000000000000, 0.3750000000000000000, 0.4375000000000000000, 0.5000000000000000000, 0.5625000000000000000, 0.6250000000000000000, 0.6875000000000000000, 0.7500000000000000000, 0.8125000000000000000, 0.8750000000000000000, 0.9375000000000000000, 0.9999968116805088014 ),
 .UNSPECIFIED. ) ;
#5582=TOROIDAL_SURFACE ( 'NONE', #18649, 7.112000000000000099, 0.7620000000000000107 ) ;
#5589=DIRECTION ( 'NONE',  ( 0.000000000000000000, -1.000000000000000000, 0.000000000000000000 ) ) ;
#5611=AXIS2_PLACEMENT_3D ( 'NONE', #2606, #9751, #7545 ) ;
#5698=EDGE_CURVE ( 'NONE', #8438, #698, #15543, .T. ) ;
#5735=CARTESIAN_POINT ( 'NONE',  ( 12.69999999999999929, -3579.494999999999891, 2272.030000000000200 ) ) ;
#5874=CARTESIAN_POINT ( 'NONE',  ( 10.18227723364999981, -3578.160723028000120, 2257.881333495000035 ) ) ;
#5963=ORIENTED_EDGE ( 'NONE', *, *, #7169, .T. ) ;
#5982=EDGE_LOOP ( 'NONE', ( #16663, #13524, #860, #21265, #8953, #12464, #21427 ) ) ;
#6046=ORIENTED_EDGE ( 'NONE', *, *, #18867, .F. ) ;
#6128=ADVANCED_FACE ( 'NONE', ( #22208 ), #6178, .F. ) ;
#6178=CYLINDRICAL_SURFACE ( 'NONE', #9629, 6.349999999999855760 ) ;
#6189=CIRCLE ( 'NONE', #5459, 0.7619999999999294005 ) ;
#6211=ORIENTED_EDGE ( 'NONE', *, *, #22539, .F. ) ;
#6222=ORIENTED_EDGE ( 'NONE', *, *, #6378, .T. ) ;
#6298=EDGE_LOOP ( 'NONE', ( #13535, #9008, #8179, #4518, #9384, #3247, #10588, #13591 ) ) ;
#6378=EDGE_CURVE ( 'NONE', #1694, #15010, #966, .T. ) ;
#6420=DIRECTION ( 'NONE',  ( 0.000000000000000000, -1.000000000000000000, 0.000000000000000000 ) ) ;
#6432=CARTESIAN_POINT ( 'NONE',  ( 15.53591867179932073, -3579.770168290938727, 2257.960586820520803 ) ) ;
#6441=VERTEX_POINT ( 'NONE', #14599 ) ;
#6444=TOROIDAL_SURFACE ( 'NONE', #1562, 7.112000000000000099, 0.7620000000000000107 ) ;
#6475=CIRCLE ( 'NONE', #8345, 11.11250000000000071 ) ;
#6484=( NAMED_UNIT ( * ) PLANE_ANGLE_UNIT ( ) SI_UNIT ( $, .RADIAN. ) );
#6501=CARTESIAN_POINT ( 'NONE',  ( 9.855200958505918152, -3579.586994900638729, 2257.962940081783472 ) ) ;
#6517=ORIENTED_EDGE ( 'NONE', *, *, #9962, .T. ) ;
#6549=CARTESIAN_POINT ( 'NONE',  ( 13.24911585008999815, -3582.290876935000142, 2257.605101898000157 ) ) ;
#6898=CARTESIAN_POINT ( 'NONE',  ( 14.03509158661000100, -3582.012285900999814, 2257.672186979000344 ) ) ;
#6936=CARTESIAN_POINT ( 'NONE',  ( 15.21772229205999949, -3578.160722075999729, 2257.881333375999930 ) ) ;
#7136=CYLINDRICAL_SURFACE ( 'NONE', #3585, 11.11249999999985860 ) ;
#7149=PRODUCT ( 'Hinge 2', 'Hinge 2', '', ( #22607 ) ) ;
#7169=EDGE_CURVE ( 'NONE', #946, #4653, #22293, .T. ) ;
#7193=CIRCLE ( 'NONE', #8310, 11.11250000000000071 ) ;
#7196=VERTEX_POINT ( 'NONE', #5121 ) ;
#7424=VECTOR ( 'NONE', #15253, 1000.000000000000000 ) ;
#7506=CARTESIAN_POINT ( 'NONE',  ( 11.12257588577000078, -3581.868010977999802, 2257.704312134999782 ) ) ;
#7516=DIRECTION ( 'NONE',  ( 0.000000000000000000, 0.000000000000000000, -1.000000000000000000 ) ) ;
#7545=DIRECTION ( 'NONE',  ( 1.000000000000000000, 0.000000000000000000, 0.000000000000000000 ) ) ;
#7546=CARTESIAN_POINT ( 'NONE',  ( 9.855200508370408841, -3579.494995334292526, 2257.962940200996854 ) ) ;
#7600=CARTESIAN_POINT ( 'NONE',  ( 12.69999999999999929, -3589.528000000000247, 2262.355140000000119 ) ) ;
#7651=ORIENTED_EDGE ( 'NONE', *, *, #22596, .T. ) ;
#7736=CARTESIAN_POINT ( 'NONE',  ( 11.36482343738000012, -3576.977758867000375, 2257.672197237000091 ) ) ;
#7826=DIRECTION ( 'NONE',  ( 0.000000000000000000, 0.000000000000000000, 1.000000000000000000 ) ) ;
#7881=VERTEX_POINT ( 'NONE', #21758 ) ;
#7899=FACE_BOUND ( 'NONE', #16294, .T. ) ;
#7932=ORIENTED_EDGE ( 'NONE', *, *, #9962, .F. ) ;
#7961=CARTESIAN_POINT ( 'NONE',  ( 15.54479972192533488, -3579.494999998566982, 2257.962943247991461 ) ) ;
#8004=DIRECTION ( 'NONE',  ( 1.000000000000000000, 0.000000000000000000, -1.224646799147353207E-16 ) ) ;
#8011=CARTESIAN_POINT ( 'NONE',  ( 15.54479972192533488, -3579.494999998566982, 2257.962943247991461 ) ) ;
#8018=FACE_OUTER_BOUND ( 'NONE', #13151, .T. ) ;
#8165=CARTESIAN_POINT ( 'NONE',  ( 12.69999999999999929, -3583.940000000000055, 2268.705139999999574 ) ) ;
#8179=ORIENTED_EDGE ( 'NONE', *, *, #4576, .T. ) ;
#8279=DIRECTION ( 'NONE',  ( 0.000000000000000000, 0.000000000000000000, 1.000000000000000000 ) ) ;
#8310=AXIS2_PLACEMENT_3D ( 'NONE', #3190, #9870, #4723 ) ;
#8345=AXIS2_PLACEMENT_3D ( 'NONE', #14444, #484, #25 ) ;
#8400=CARTESIAN_POINT ( 'NONE',  ( 12.69999999999999929, -3590.289999999999964, 2268.705139999999574 ) ) ;
#8438=VERTEX_POINT ( 'NONE', #8011 ) ;
#8442=VECTOR ( 'NONE', #9521, 1000.000000000000000 ) ;
#8574=CARTESIAN_POINT ( 'NONE',  ( 12.69999999999999929, -3576.650200000000041, 2257.592639999999847 ) ) ;
#8628=DIRECTION ( 'NONE',  ( 1.000000000000000000, 0.000000000000000000, 0.000000000000000000 ) ) ;
#8646=CARTESIAN_POINT ( 'NONE',  ( 13.78126912685999983, -3582.131243251999877, 2257.644351290000031 ) ) ;
#8802=CARTESIAN_POINT ( 'NONE',  ( 15.07358448401000217, -3577.918427944000086, 2257.848701151000114 ) ) ;
#8887=LINE ( 'NONE', #14279, #10862 ) ;
#8917=CARTESIAN_POINT ( 'NONE',  ( 15.33662675678000120, -3578.414664496000114, 2257.909780506000061 ) ) ;
#8926=B_SPLINE_CURVE_WITH_KNOTS ( 'NONE', 3,
 ( #12551, #6501, #9037, #16183, #136, #1206, #14551, #2125, #9156, #2238, #20280, #7506, #10908, #21690, #19819, #12667, #21916, #3994, #19934 ),
 .UNSPECIFIED., .F., .F.,
 ( 4, 1, 1, 1, 1, 1, 1, 1, 1, 1, 1, 1, 1, 1, 1, 1, 4 ),
 ( 3.168591426078754222E-06, 0.06250000000000000000, 0.1250000000000000000, 0.1875000000000000000, 0.2500000000000000000, 0.3125000000000000000, 0.3750000000000000000, 0.4375000000000000000, 0.5000000000000000000, 0.5625000000000000000, 0.6250000000000000000, 0.6875000000000000000, 0.7500000000000000000, 0.8125000000000000000, 0.8750000000000000000, 0.9375000000000000000, 1.000000000000000000 ),
 .UNSPECIFIED. ) ;
#8953=ORIENTED_EDGE ( 'NONE', *, *, #17655, .F. ) ;
#9002=ORIENTED_EDGE ( 'NONE', *, *, #12510, .T. ) ;
#9007=DIRECTION ( 'NONE',  ( 0.000000000000000000, -1.000000000000000000, 0.000000000000000000 ) ) ;
#9008=ORIENTED_EDGE ( 'NONE', *, *, #2624, .F. ) ;
#9035=CARTESIAN_POINT ( 'NONE',  ( 15.53593155406000115, -3579.219969270000092, 2257.960590233999937 ) ) ;
#9037=CARTESIAN_POINT ( 'NONE',  ( 9.864080040025308804, -3579.770148078739112, 2257.960588549625299 ) ) ;
#9145=CIRCLE ( 'NONE', #10252, 11.11250000000000071 ) ;
#9156=CARTESIAN_POINT ( 'NONE',  ( 10.49449033964999956, -3581.299265058999936, 2257.813191440000082 ) ) ;
#9161=AXIS2_PLACEMENT_3D ( 'NONE', #8165, #11784, #18937 ) ;
#9245=EDGE_CURVE ( 'NONE', #18657, #8438, #5488, .T. ) ;
#9266=CARTESIAN_POINT ( 'NONE',  ( 10.06337286646999907, -3578.414665316000082, 2257.909780569999839 ) ) ;
#9325=ORIENTED_EDGE ( 'NONE', *, *, #15164, .T. ) ;
#9359=CARTESIAN_POINT ( 'NONE',  ( 12.69999999999999929, -3579.494999999999891, 2272.030000000000200 ) ) ;
#9380=ORIENTED_EDGE ( 'NONE', *, *, #22596, .F. ) ;
#9384=ORIENTED_EDGE ( 'NONE', *, *, #14297, .T. ) ;
#9476=LINE ( 'NONE', #15100, #22161 ) ;
#9521=DIRECTION ( 'NONE',  ( 0.000000000000000000, -1.000000000000000000, 0.000000000000000000 ) ) ;
#9581=AXIS2_PLACEMENT_3D ( 'NONE', #10542, #22600, #20861 ) ;
#9603=CARTESIAN_POINT ( 'NONE',  ( 9.855200508358999301, -3579.403078924000511, 2257.962940201000038 ) ) ;
#9629=AXIS2_PLACEMENT_3D ( 'NONE', #9901, #878, #4871 ) ;
#9642=DIRECTION ( 'NONE',  ( 0.000000000000000000, 0.000000000000000000, -1.000000000000000000 ) ) ;
#9653=DIRECTION ( 'NONE',  ( -1.000000000000000000, 0.000000000000000000, 0.000000000000000000 ) ) ;
#9711=CARTESIAN_POINT ( 'NONE',  ( 12.69999999999999929, -3576.650200000000041, 2257.592639999999847 ) ) ;
#9751=DIRECTION ( 'NONE',  ( 0.000000000000000000, 0.000000000000000000, 1.000000000000000000 ) ) ;
#9824=CARTESIAN_POINT ( 'NONE',  ( 12.69999999999999929, -3570.287499999999909, 2268.705139999999574 ) ) ;
#9842=EDGE_CURVE ( 'NONE', #18657, #6441, #941, .T. ) ;
#9870=DIRECTION ( 'NONE',  ( 0.000000000000000000, -1.000000000000000000, 0.000000000000000000 ) ) ;
#9901=CARTESIAN_POINT ( 'NONE',  ( 12.69999999999999929, -3583.940000000000055, 2268.705139999999574 ) ) ;
#9936=DIRECTION ( 'NONE',  ( 1.000000000000000000, 0.000000000000000000, 3.996303350731721563E-14 ) ) ;
#9938=DIRECTION ( 'NONE',  ( 0.000000000000000000, -1.000000000000000000, 0.000000000000000000 ) ) ;
#9962=EDGE_CURVE ( 'NONE', #15423, #14057, #2880, .T. ) ;
#10205=ORIENTED_EDGE ( 'NONE', *, *, #9842, .F. ) ;
#10252=AXIS2_PLACEMENT_3D ( 'NONE', #2792, #4546, #9936 ) ;
#10281=CARTESIAN_POINT ( 'NONE',  ( 14.90539642439000012, -3581.299404879999656, 2257.813168336999752 ) ) ;
#10542=CARTESIAN_POINT ( 'NONE',  ( 12.69999999999999929, -3589.528000000000247, 2268.705139999999574 ) ) ;
#10588=ORIENTED_EDGE ( 'NONE', *, *, #9842, .T. ) ;
#10650=CARTESIAN_POINT ( 'NONE',  ( 12.69999999999999929, -3583.940000000000055, 2268.705139999999574 ) ) ;
#10680=ORIENTED_EDGE ( 'NONE', *, *, #5698, .T. ) ;
#10736=CYLINDRICAL_SURFACE ( 'NONE', #21971, 6.349999999999855760 ) ;
#10740=CARTESIAN_POINT ( 'NONE',  ( 9.855199999999999960, -3579.494999999999891, 2272.030000000000200 ) ) ;
#10862=VECTOR ( 'NONE', #19659, 1000.000000000000000 ) ;
#10866=ADVANCED_FACE ( 'NONE', ( #2677 ), #22239, .T. ) ;
#10890=EDGE_LOOP ( 'NONE', ( #20588, #6211, #9002, #18831 ) ) ;
#10908=CARTESIAN_POINT ( 'NONE',  ( 11.36465921565999970, -3582.012152740000147, 2257.672217410000030 ) ) ;
#11137=ORIENTED_EDGE ( 'NONE', *, *, #20942, .T. ) ;
#11155=ADVANCED_FACE ( 'NONE', ( #12295 ), #7136, .T. ) ;
#11166=ADVANCED_FACE ( 'NONE', ( #20024 ), #14520, .F. ) ;
#11224=PLANE ( 'NONE',  #3564 ) ;
#11271=ADVANCED_FACE ( 'NONE', ( #16607 ), #18135, .F. ) ;
#11351=CARTESIAN_POINT ( 'NONE',  ( 11.12270644712000056, -3577.121901140999853, 2257.704293189000055 ) ) ;
#11427=EDGE_CURVE ( 'NONE', #14057, #15423, #2092, .T. ) ;
#11466=CARTESIAN_POINT ( 'NONE',  ( 15.54479972196000048, -3579.494990611520279, 2257.962943248000101 ) ) ;
#11515=DIRECTION ( 'NONE',  ( 0.000000000000000000, 0.000000000000000000, -1.000000000000000000 ) ) ;
#11680=CARTESIAN_POINT ( 'NONE',  ( 15.33658054938999982, -3580.575448001000041, 2257.909769185999721 ) ) ;
#11708=CLOSED_SHELL ( 'NONE', ( #11155, #1488, #6128, #11271, #11166, #21276, #15945, #18790, #3502, #22445, #5239, #10866 ) ) ;
#11784=DIRECTION ( 'NONE',  ( 0.000000000000000000, -1.000000000000000000, 0.000000000000000000 ) ) ;
#11805=CARTESIAN_POINT ( 'NONE',  ( 12.97541421502999981, -3582.330907204000141, 2257.594921553999939 ) ) ;
#11813=EDGE_CURVE ( 'NONE', #7196, #18657, #8926, .T. ) ;
#11927=CARTESIAN_POINT ( 'NONE',  ( 13.51841762737000074, -3582.224253381999915, 2257.621745511999961 ) ) ;
#12082=CARTESIAN_POINT ( 'NONE',  ( 14.27729191008000065, -3577.121900051000011, 2257.704292951999832 ) ) ;
#12193=CARTESIAN_POINT ( 'NONE',  ( 12.69999999999999929, -3590.289999999999964, 2268.705139999999574 ) ) ;
#12261=CARTESIAN_POINT ( 'NONE',  ( 12.69999999999999929, -3589.528000000000247, 2268.705139999999574 ) ) ;
#12276=ORIENTED_EDGE ( 'NONE', *, *, #18326, .T. ) ;
#12295=FACE_OUTER_BOUND ( 'NONE', #784, .T. ) ;
#12383=DIRECTION ( 'NONE',  ( -1.000000000000000000, -0.000000000000000000, -0.000000000000000000 ) ) ;
#12464=ORIENTED_EDGE ( 'NONE', *, *, #19418, .F. ) ;
#12493=APPLICATION_CONTEXT ( 'configuration controlled 3d designs of mechanical parts and assemblies' ) ;
#12510=EDGE_CURVE ( 'NONE', #7881, #15010, #886, .T. ) ;
#12551=CARTESIAN_POINT ( 'NONE',  ( 9.855200508393231473, -3579.494999998446929, 2257.962940200991852 ) ) ;
#12588=CARTESIAN_POINT ( 'NONE',  ( 9.855199999999999960, -3579.494999999999891, 2272.030000000000200 ) ) ;
#12629=CARTESIAN_POINT ( 'NONE',  ( 12.70000000000000107, -3590.289999999999964, 2275.817139999999654 ) ) ;
#12639=DIRECTION ( 'NONE',  ( 0.000000000000000000, -1.000000000000000000, 0.000000000000000000 ) ) ;
#12667=CARTESIAN_POINT ( 'NONE',  ( 12.15052771711000013, -3582.290804947000197, 2257.605120077999800 ) ) ;
#12751=CARTESIAN_POINT ( 'NONE',  ( 12.69999999999999929, -3570.287499999999909, 2268.705139999999574 ) ) ;
#12752=CARTESIAN_POINT ( 'NONE',  ( 12.70000000000000107, -3570.287499999999909, 2279.817639999999756 ) ) ;
#12791=AXIS2_PLACEMENT_3D ( 'NONE', #4380, #11515, #9653 ) ;
#12840=LINE ( 'NONE', #10740, #22281 ) ;
#12859=CARTESIAN_POINT ( 'NONE',  ( 15.54479999999999862, -3579.494999999999891, 2272.030000000000200 ) ) ;
#12889=CARTESIAN_POINT ( 'NONE',  ( 9.970475488813999476, -3578.677501247999771, 2257.932973791000222 ) ) ;
#12971=VERTEX_POINT ( 'NONE', #22193 ) ;
#13044=ORIENTED_EDGE ( 'NONE', *, *, #12510, .F. ) ;
#13151=EDGE_LOOP ( 'NONE', ( #12276, #23164 ) ) ;
#13255=SHAPE_REPRESENTATION ( 'Hinge 2', ( #5611 ), #1485 ) ;
#13287=ORIENTED_EDGE ( 'NONE', *, *, #18867, .T. ) ;
#13299=VECTOR ( 'NONE', #6420, 1000.000000000000000 ) ;
#13398=CYLINDRICAL_SURFACE ( 'NONE', #12791, 2.844799999999999773 ) ;
#13410=EDGE_CURVE ( 'NONE', #15423, #1694, #6189, .T. ) ;
#13471=FACE_OUTER_BOUND ( 'NONE', #20420, .T. ) ;
#13515=MANIFOLD_SOLID_BREP ( 'SOLID2-13[1]', #11708 ) ;
#13524=ORIENTED_EDGE ( 'NONE', *, *, #7169, .F. ) ;
#13530=CARTESIAN_POINT ( 'NONE',  ( 12.69999999999999929, -3570.287499999999909, 2257.592639999999847 ) ) ;
#13535=ORIENTED_EDGE ( 'NONE', *, *, #20050, .F. ) ;
#13569=CARTESIAN_POINT ( 'NONE',  ( 15.54479926893309027, -3579.587001414151928, 2257.962943127797644 ) ) ;
#13591=ORIENTED_EDGE ( 'NONE', *, *, #16111, .F. ) ;
#13619=ORIENTED_EDGE ( 'NONE', *, *, #9245, .T. ) ;
#13631=EDGE_LOOP ( 'NONE', ( #19444, #9325, #13915, #19385, #3131 ) ) ;
#13643=CARTESIAN_POINT ( 'NONE',  ( 12.69999999999999929, -3579.494999999999891, 2272.030000000000200 ) ) ;
#13688=CARTESIAN_POINT ( 'NONE',  ( 15.49598722424000030, -3580.043501552999714, 2257.950090894999903 ) ) ;
#13749=( NAMED_UNIT ( * ) SI_UNIT ( $, .STERADIAN. ) SOLID_ANGLE_UNIT ( ) );
#13809=CARTESIAN_POINT ( 'NONE',  ( 14.50480255619999959, -3581.700066511000387, 2257.739429448999999 ) ) ;
#13821=DIRECTION ( 'NONE',  ( 0.000000000000000000, 0.000000000000000000, -1.000000000000000000 ) ) ;
#13900=VERTEX_POINT ( 'NONE', #15674 ) ;
#13915=ORIENTED_EDGE ( 'NONE', *, *, #9245, .F. ) ;
#14022=CARTESIAN_POINT ( 'NONE',  ( 12.69999999999999929, -3570.287499999999909, 2268.705139999999574 ) ) ;
#14023=DIRECTION ( 'NONE',  ( 0.000000000000000000, 0.000000000000000000, -1.000000000000000000 ) ) ;
#14057=VERTEX_POINT ( 'NONE', #20554 ) ;
#14083=AXIS2_PLACEMENT_3D ( 'NONE', #12261, #19406, #3340 ) ;
#14130=VERTEX_POINT ( 'NONE', #13530 ) ;
#14156=DIRECTION ( 'NONE',  ( 0.000000000000000000, 0.000000000000000000, -1.000000000000000000 ) ) ;
#14270=VERTEX_POINT ( 'NONE', #15523 ) ;
#14279=CARTESIAN_POINT ( 'NONE',  ( 12.69999999999999929, -3570.287499999999909, 2257.592639999999847 ) ) ;
#14297=EDGE_CURVE ( 'NONE', #14270, #7196, #1569, .T. ) ;
#14399=CIRCLE ( 'NONE', #15886, 11.11250000000000071 ) ;
#14404=ORIENTED_EDGE ( 'NONE', *, *, #1797, .T. ) ;
#14429=CARTESIAN_POINT ( 'NONE',  ( 14.71514678359000072, -3577.480332084000111, 2257.776246897999954 ) ) ;
#14444=CARTESIAN_POINT ( 'NONE',  ( 12.69999999999999929, -3570.287499999999909, 2268.705139999999574 ) ) ;
#14520=PLANE ( 'NONE',  #18920 ) ;
#14551=CARTESIAN_POINT ( 'NONE',  ( 10.18227454630999951, -3580.829269783999734, 2257.881334183000035 ) ) ;
#14599=CARTESIAN_POINT ( 'NONE',  ( 12.69999999999999929, -3590.289999999999964, 2257.592639999999847 ) ) ;
#14644=CIRCLE ( 'NONE', #19503, 2.844799999999999773 ) ;
#14654=CARTESIAN_POINT ( 'NONE',  ( 10.89511648704999836, -3577.289999577000344, 2257.739442794000297 ) ) ;
#14713=ORIENTED_EDGE ( 'NONE', *, *, #20050, .T. ) ;
#14754=FACE_OUTER_BOUND ( 'NONE', #20545, .T. ) ;
#14789=ORIENTED_EDGE ( 'NONE', *, *, #11427, .F. ) ;
#14888=CARTESIAN_POINT ( 'NONE',  ( 10.49453184709999931, -3577.690682589000062, 2257.813182895999944 ) ) ;
#15010=VERTEX_POINT ( 'NONE', #7600 ) ;
#15081=FACE_OUTER_BOUND ( 'NONE', #19269, .T. ) ;
#15100=CARTESIAN_POINT ( 'NONE',  ( 15.54479999999999862, -3579.494999999999891, 2272.030000000000200 ) ) ;
#15164=EDGE_CURVE ( 'NONE', #4653, #8438, #9476, .T. ) ;
#15253=DIRECTION ( 'NONE',  ( 0.000000000000000000, -1.000000000000000000, 0.000000000000000000 ) ) ;
#15282=ORIENTED_EDGE ( 'NONE', *, *, #4576, .F. ) ;
#15330=CARTESIAN_POINT ( 'NONE',  ( 12.70000020906999971, -3582.339800010000090, 2257.592639999999847 ) ) ;
#15340=DIRECTION ( 'NONE',  ( 0.000000000000000000, 0.000000000000000000, -1.000000000000000000 ) ) ;
#15423=VERTEX_POINT ( 'NONE', #12629 ) ;
#15523=CARTESIAN_POINT ( 'NONE',  ( 9.855200508358999301, -3579.494986006000545, 2257.962940201000038 ) ) ;
#15543=B_SPLINE_CURVE_WITH_KNOTS ( 'NONE', 3,
 ( #7961, #4327, #11466, #18618 ),
 .UNSPECIFIED., .F., .F.,
 ( 4, 4 ),
 ( 0.9999968116805088014, 1.000000000000000000 ),
 .UNSPECIFIED. ) ;
#15563=VECTOR ( 'NONE', #9007, 1000.000000000000000 ) ;
#15568=AXIS2_PLACEMENT_3D ( 'NONE', #5735, #16268, #21663 ) ;
#15674=CARTESIAN_POINT ( 'NONE',  ( 12.69999999999999929, -3583.940000000000055, 2275.055139999999483 ) ) ;
#15703=ORIENTED_EDGE ( 'NONE', *, *, #19418, .T. ) ;
#15786=FACE_OUTER_BOUND ( 'NONE', #2096, .T. ) ;
#15840=ORIENTED_EDGE ( 'NONE', *, *, #3061, .T. ) ;
#15886=AXIS2_PLACEMENT_3D ( 'NONE', #14022, #19407, #5232 ) ;
#15945=ADVANCED_FACE ( 'NONE', ( #2396 ), #13398, .F. ) ;
#15982=AXIS2_PLACEMENT_3D ( 'NONE', #12193, #1636, #19344 ) ;
#16062=CARTESIAN_POINT ( 'NONE',  ( 14.90546723228000126, -3577.690681480999956, 2257.813182709000102 ) ) ;
#16111=EDGE_CURVE ( 'NONE', #21367, #6441, #7193, .T. ) ;
#16125=CARTESIAN_POINT ( 'NONE',  ( 12.69999999999999929, -3583.940000000000055, 2268.705139999999574 ) ) ;
#16183=CARTESIAN_POINT ( 'NONE',  ( 9.904004635912999177, -3580.043455317999815, 2257.950092655999924 ) ) ;
#16268=DIRECTION ( 'NONE',  ( 0.000000000000000000, 0.000000000000000000, -1.000000000000000000 ) ) ;
#16294=EDGE_LOOP ( 'NONE', ( #365, #6517 ) ) ;
#16403=CARTESIAN_POINT ( 'NONE',  ( 12.42449270472999956, -3576.659101290000308, 2257.594923725999706 ) ) ;
#16607=FACE_OUTER_BOUND ( 'NONE', #13631, .T. ) ;
#16625=CARTESIAN_POINT ( 'NONE',  ( 12.60791899384999937, -3576.650200000000041, 2257.592639999999847 ) ) ;
#16663=ORIENTED_EDGE ( 'NONE', *, *, #15164, .F. ) ;
#16669=VERTEX_POINT ( 'NONE', #324 ) ;
#16728=CARTESIAN_POINT ( 'NONE',  ( 12.69999999999999929, -3583.940000000000055, 2262.355140000000119 ) ) ;
#16741=UNCERTAINTY_MEASURE_WITH_UNIT (LENGTH_MEASURE( 1.000000000000000082E-05 ), #21126, 'distance_accuracy_value', 'NONE');
#16888=EDGE_LOOP ( 'NONE', ( #114, #11137, #4274, #13044 ) ) ;
#17023=CARTESIAN_POINT ( 'NONE',  ( 12.69999999999999929, -3590.289999999999964, 2268.705139999999574 ) ) ;
#17413=EDGE_LOOP ( 'NONE', ( #2289, #13287 ) ) ;
#17490=CIRCLE ( 'NONE', #9581, 6.349999999999855760 ) ;
#17579=CARTESIAN_POINT ( 'NONE',  ( 12.79208108087000006, -3576.650200000000041, 2257.592639999999847 ) ) ;
#17655=EDGE_CURVE ( 'NONE', #12971, #14270, #4505, .T. ) ;
#17672=ORIENTED_EDGE ( 'NONE', *, *, #22539, .T. ) ;
#17819=AXIS2_PLACEMENT_3D ( 'NONE', #9824, #9938, #15340 ) ;
#17908=DIRECTION ( 'NONE',  ( 0.000000000000000000, 0.000000000000000000, -1.000000000000000000 ) ) ;
#17977=CARTESIAN_POINT ( 'NONE',  ( 9.855200508393231473, -3579.494999998446929, 2257.962940200991852 ) ) ;
#18135=CYLINDRICAL_SURFACE ( 'NONE', #15568, 2.844799999999999773 ) ;
#18197=AXIS2_PLACEMENT_3D ( 'NONE', #3345, #14023, #8628 ) ;
#18326=EDGE_CURVE ( 'NONE', #6441, #21367, #9145, .T. ) ;
#18480=LINE ( 'NONE', #12752, #15563 ) ;
#18618=CARTESIAN_POINT ( 'NONE',  ( 15.54479972196000048, -3579.494985918000111, 2257.962943248000101 ) ) ;
#18624=AXIS2_PLACEMENT_3D ( 'NONE', #17023, #737, #2615 ) ;
#18649=AXIS2_PLACEMENT_3D ( 'NONE', #20828, #4771, #2897 ) ;
#18652=LINE ( 'NONE', #22389, #8442 ) ;
#18657=VERTEX_POINT ( 'NONE', #3606 ) ;
#18667=CIRCLE ( 'NONE', #2963, 6.349999999999855760 ) ;
#18790=ADVANCED_FACE ( 'NONE', ( #15081 ), #1004, .T. ) ;
#18831=ORIENTED_EDGE ( 'NONE', *, *, #6378, .F. ) ;
#18867=EDGE_CURVE ( 'NONE', #16669, #14130, #14399, .T. ) ;
#18871=SHAPE_DEFINITION_REPRESENTATION ( #1316, #13255 ) ;
#18920=AXIS2_PLACEMENT_3D ( 'NONE', #12751, #12639, #17908 ) ;
#18937=DIRECTION ( 'NONE',  ( 0.000000000000000000, 0.000000000000000000, -1.000000000000000000 ) ) ;
#19011=ORIENTED_EDGE ( 'NONE', *, *, #13410, .F. ) ;
#19015=( LENGTH_UNIT ( ) NAMED_UNIT ( * ) SI_UNIT ( .MILLI., .METRE. ) );
#19194=CARTESIAN_POINT ( 'NONE',  ( 12.79204376678999999, -3582.339799989999847, 2257.592639999999847 ) ) ;
#19235=CARTESIAN_POINT ( 'NONE',  ( 13.78135004281000064, -3576.858789906999846, 2257.644359223000265 ) ) ;
#19269=EDGE_LOOP ( 'NONE', ( #17672, #14404 ) ) ;
#19333=CARTESIAN_POINT ( 'NONE',  ( 12.69999999999999929, -3589.528000000000247, 2275.055139999999483 ) ) ;
#19344=DIRECTION ( 'NONE',  ( 0.000000000000000000, 0.000000000000000000, 1.000000000000000000 ) ) ;
#19352=CARTESIAN_POINT ( 'NONE',  ( 14.03517516284999900, -3576.977758144000290, 2257.672197071000028 ) ) ;
#19385=ORIENTED_EDGE ( 'NONE', *, *, #11813, .F. ) ;
#19406=DIRECTION ( 'NONE',  ( 0.000000000000000000, 1.000000000000000000, 0.000000000000000000 ) ) ;
#19407=DIRECTION ( 'NONE',  ( 0.000000000000000000, 1.000000000000000000, 0.000000000000000000 ) ) ;
#19418=EDGE_CURVE ( 'NONE', #698, #12971, #19539, .T. ) ;
#19426=ADVANCED_BREP_SHAPE_REPRESENTATION ( '', ( #13515, #5611 ), #1485 ) ;
#19438=CARTESIAN_POINT ( 'NONE',  ( 12.69999999999999929, -3570.287499999999909, 2268.705139999999574 ) ) ;
#19444=ORIENTED_EDGE ( 'NONE', *, *, #742, .F. ) ;
#19466=CARTESIAN_POINT ( 'NONE',  ( 13.51849986531999903, -3576.765770756000165, 2257.621751478000078 ) ) ;
#19503=AXIS2_PLACEMENT_3D ( 'NONE', #13643, #22079, #20446 ) ;
#19539=B_SPLINE_CURVE_WITH_KNOTS ( 'NONE', 3,
 ( #1645, #1881, #9035, #134, #1773, #8917, #6936, #8802, #16062, #14429, #21580, #12082, #19352, #19235, #19466, #3168, #1418, #17579, #8574 ),
 .UNSPECIFIED., .F., .F.,
 ( 4, 1, 1, 1, 1, 1, 1, 1, 1, 1, 1, 1, 1, 1, 1, 1, 4 ),
 ( 0.000000000000000000, 0.06250000000000000000, 0.1250000000000000000, 0.1875000000000000000, 0.2500000000000000000, 0.3125000000000000000, 0.3750000000000000000, 0.4375000000000000000, 0.5000000000000000000, 0.5625000000000000000, 0.6250000000000000000, 0.6875000000000000000, 0.7500000000000000000, 0.8125000000000000000, 0.8750000000000000000, 0.9375000000000000000, 1.000000000000000000 ),
 .UNSPECIFIED. ) ;
#19659=DIRECTION ( 'NONE',  ( 0.000000000000000000, -1.000000000000000000, 0.000000000000000000 ) ) ;
#19748=CARTESIAN_POINT ( 'NONE',  ( 9.855200508358999301, -3579.494990670147217, 2257.962940201000038 ) ) ;
#19819=CARTESIAN_POINT ( 'NONE',  ( 11.88126810894999963, -3582.224158427000020, 2257.621768944999985 ) ) ;
#19934=CARTESIAN_POINT ( 'NONE',  ( 12.70000020906999971, -3582.339800010000090, 2257.592639999999847 ) ) ;
#20024=FACE_OUTER_BOUND ( 'NONE', #17413, .T. ) ;
#20035=UNCERTAINTY_MEASURE_WITH_UNIT (LENGTH_MEASURE( 1.000000000000000082E-05 ), #19015, 'distance_accuracy_value', 'NONE');
#20048=CARTESIAN_POINT ( 'NONE',  ( 11.88149704131999940, -3576.765771669000060, 2257.621751704000417 ) ) ;
#20050=EDGE_CURVE ( 'NONE', #16669, #21367, #18480, .T. ) ;
#20271=CARTESIAN_POINT ( 'NONE',  ( 12.15081356636999921, -3576.699137309000434, 2257.605105499000274 ) ) ;
#20280=CARTESIAN_POINT ( 'NONE',  ( 10.89501796730999850, -3581.699918485000126, 2257.739459224999791 ) ) ;
#20376=CARTESIAN_POINT ( 'NONE',  ( 10.68485228337000059, -3577.480333023000185, 2257.776247070999943 ) ) ;
#20388=ORIENTED_EDGE ( 'NONE', *, *, #742, .T. ) ;
#20397=EDGE_CURVE ( 'NONE', #946, #7196, #12840, .T. ) ;
#20420=EDGE_LOOP ( 'NONE', ( #7932, #3678, #6222, #9380 ) ) ;
#20446=DIRECTION ( 'NONE',  ( 1.000000000000000000, 0.000000000000000000, 0.000000000000000000 ) ) ;
#20503=PRODUCT_DEFINITION ( 'UNKNOWN', '', #3730, #4563 ) ;
#20545=EDGE_LOOP ( 'NONE', ( #5963, #20388 ) ) ;
#20554=CARTESIAN_POINT ( 'NONE',  ( 12.69999999999999929, -3590.289999999999964, 2261.593139999999948 ) ) ;
#20588=ORIENTED_EDGE ( 'NONE', *, *, #20942, .F. ) ;
#20710=CARTESIAN_POINT ( 'NONE',  ( 15.54479972192533488, -3579.494999998566982, 2257.962943247991461 ) ) ;
#20828=CARTESIAN_POINT ( 'NONE',  ( 12.69999999999999929, -3589.528000000000247, 2268.705139999999574 ) ) ;
#20849=DIRECTION ( 'NONE',  ( 0.000000000000000000, -1.000000000000000000, 0.000000000000000000 ) ) ;
#20861=DIRECTION ( 'NONE',  ( 0.000000000000000000, 0.000000000000000000, 1.000000000000000000 ) ) ;
#20942=EDGE_CURVE ( 'NONE', #13900, #1694, #18652, .T. ) ;
#21126=( LENGTH_UNIT ( ) NAMED_UNIT ( * ) SI_UNIT ( .MILLI., .METRE. ) );
#21265=ORIENTED_EDGE ( 'NONE', *, *, #14297, .F. ) ;
#21276=ADVANCED_FACE ( 'NONE', ( #14754 ), #11224, .F. ) ;
#21367=VERTEX_POINT ( 'NONE', #2894 ) ;
#21427=ORIENTED_EDGE ( 'NONE', *, *, #5698, .F. ) ;
#21580=CARTESIAN_POINT ( 'NONE',  ( 14.50488223892000050, -3577.289998514000217, 2257.739442581999810 ) ) ;
#21663=DIRECTION ( 'NONE',  ( -1.000000000000000000, 0.000000000000000000, 0.000000000000000000 ) ) ;
#21673=AXIS2_PLACEMENT_3D ( 'NONE', #23036, #12383, #3590 ) ;
#21690=CARTESIAN_POINT ( 'NONE',  ( 11.61844525849999954, -3582.131125288000021, 2257.644379465999918 ) ) ;
#21758=CARTESIAN_POINT ( 'NONE',  ( 12.69999999999999929, -3583.940000000000055, 2262.355140000000119 ) ) ;
#21795=CARTESIAN_POINT ( 'NONE',  ( 9.864068217991999177, -3579.219970543999807, 2257.960591680000107 ) ) ;
#21916=CARTESIAN_POINT ( 'NONE',  ( 12.42421805959000025, -3582.330875907999598, 2257.594929573999707 ) ) ;
#21971=AXIS2_PLACEMENT_3D ( 'NONE', #16125, #5589, #3695 ) ;
#22017=CARTESIAN_POINT ( 'NONE',  ( 9.855200508358999301, -3579.494986006000545, 2257.962940201000038 ) ) ;
#22041=CARTESIAN_POINT ( 'NONE',  ( 12.69999999999999929, -3570.287499999999909, 2257.592639999999847 ) ) ;
#22079=DIRECTION ( 'NONE',  ( 0.000000000000000000, 0.000000000000000000, -1.000000000000000000 ) ) ;
#22111=DIRECTION ( 'NONE',  ( 1.000000000000000000, 0.000000000000000000, 0.000000000000000000 ) ) ;
#22161=VECTOR ( 'NONE', #22226, 1000.000000000000000 ) ;
#22193=CARTESIAN_POINT ( 'NONE',  ( 12.69999999999999929, -3576.650200000000041, 2257.592639999999847 ) ) ;
#22208=FACE_OUTER_BOUND ( 'NONE', #16888, .T. ) ;
#22226=DIRECTION ( 'NONE',  ( 0.000000000000000000, 0.000000000000000000, -1.000000000000000000 ) ) ;
#22239=CYLINDRICAL_SURFACE ( 'NONE', #17819, 11.11249999999985860 ) ;
#22246=DIRECTION ( 'NONE',  ( 0.000000000000000000, 0.000000000000000000, -1.000000000000000000 ) ) ;
#22281=VECTOR ( 'NONE', #532, 1000.000000000000000 ) ;
#22293=CIRCLE ( 'NONE', #18197, 2.844799999999999773 ) ;
#22367=DIRECTION ( 'NONE',  ( 0.000000000000000000, -1.000000000000000000, 0.000000000000000000 ) ) ;
#22389=CARTESIAN_POINT ( 'NONE',  ( 12.69999999999999929, -3583.940000000000055, 2275.055139999999483 ) ) ;
#22403=CIRCLE ( 'NONE', #21673, 0.7619999999999294005 ) ;
#22418=CARTESIAN_POINT ( 'NONE',  ( 15.54479972196000048, -3579.494985918000111, 2257.962943248000101 ) ) ;
#22445=ADVANCED_FACE ( 'NONE', ( #15786 ), #5582, .T. ) ;
#22459=CARTESIAN_POINT ( 'NONE',  ( 15.42948858069999929, -3580.312618740999824, 2257.932964559000084 ) ) ;
#22469=APPLICATION_CONTEXT ( 'configuration controlled 3d designs of mechanical parts and assemblies' ) ;
#22539=EDGE_CURVE ( 'NONE', #7881, #13900, #18667, .T. ) ;
#22596=EDGE_CURVE ( 'NONE', #14057, #15010, #22403, .T. ) ;
#22600=DIRECTION ( 'NONE',  ( 0.000000000000000000, 1.000000000000000000, 0.000000000000000000 ) ) ;
#22607=PRODUCT_CONTEXT ( 'NONE', #22469, 'mechanical' ) ;
#22774=CARTESIAN_POINT ( 'NONE',  ( 9.855200508358999301, -3579.494986006000545, 2257.962940201000038 ) ) ;
#22878=CIRCLE ( 'NONE', #4192, 6.349999999999855760 ) ;
#23036=CARTESIAN_POINT ( 'NONE',  ( 12.69999999999999929, -3589.528000000000247, 2261.593139999999948 ) ) ;
#23094=( NAMED_UNIT ( * ) SI_UNIT ( $, .STERADIAN. ) SOLID_ANGLE_UNIT ( ) );
#23164=ORIENTED_EDGE ( 'NONE', *, *, #16111, .T. ) ;
#23194=COLOUR_RGB('Sky Blue',0.24,0.69,0.87);
#23195=FILL_AREA_STYLE_COLOUR('',#23194);
#23196=FILL_AREA_STYLE('',(#23195));
#23197=SURFACE_STYLE_FILL_AREA(#23196);
#23198=SURFACE_SIDE_STYLE('',(#23197));
#23199=SURFACE_STYLE_USAGE(.BOTH.,#23198);
#23200=PRESENTATION_STYLE_ASSIGNMENT((#23199));
#23222=STYLED_ITEM('',(#23200),#13515);
#23237=MECHANICAL_DESIGN_GEOMETRIC_PRESENTATION_REPRESENTATION('',(#23222),#2257);
ENDSEC;
END-ISO-10303-21;
